ISO-10303-21;
HEADER;
/* Generated by software containing ST-Developer
 * from STEP Tools, Inc. (www.steptools.com) 
 */

FILE_DESCRIPTION(
/* description */ ('Rigid flange shaft coupling assembly'),
/* implementation_level */ '2;1');

FILE_NAME(
/* name */ 'Bonded pad (1).step',
/* time_stamp */ '2026-10-27T10:47:16-07:00',
/* author */ (''),
/* organization */ (''),
/* preprocessor_version */ 'ST-DEVELOPER v20.2',
/* originating_system */ 'Autodesk Translation Framework v15.17.0.0',
/* authorisation */ '');

FILE_SCHEMA (('AUTOMOTIVE_DESIGN { 1 0 10303 214 3 1 1 }'));
ENDSEC;

DATA;
#10=MECHANICAL_DESIGN_GEOMETRIC_PRESENTATION_REPRESENTATION('',(#400),#9141);
#344=SHAPE_REPRESENTATION_RELATIONSHIP('SRR','None',#9278,#372);
#372=ADVANCED_BREP_SHAPE_REPRESENTATION('',(#429),#9113);
#400=STYLED_ITEM('',(#9514),#429);
#429=MANIFOLD_SOLID_BREP('Body1',#4754);
#582=PLANE('',#5122);
#583=PLANE('',#5123);
#584=PLANE('',#5124);
#585=PLANE('',#5125);
#586=PLANE('',#5126);
#587=PLANE('',#5127);
#760=FACE_OUTER_BOUND('',#1040,.T.);
#761=FACE_OUTER_BOUND('',#1041,.T.);
#762=FACE_OUTER_BOUND('',#1042,.T.);
#763=FACE_OUTER_BOUND('',#1043,.T.);
#764=FACE_OUTER_BOUND('',#1044,.T.);
#765=FACE_OUTER_BOUND('',#1045,.T.);
#1040=EDGE_LOOP('',(#3315,#3316,#3317,#3318));
#1041=EDGE_LOOP('',(#3319,#3320,#3321,#3322));
#1042=EDGE_LOOP('',(#3323,#3324,#3325,#3326));
#1043=EDGE_LOOP('',(#3327,#3328,#3329,#3330));
#1044=EDGE_LOOP('',(#3331,#3332,#3333,#3334));
#1045=EDGE_LOOP('',(#3335,#3336,#3337,#3338));
#1433=LINE('',#7169,#1778);
#1434=LINE('',#7171,#1779);
#1435=LINE('',#7173,#1780);
#1436=LINE('',#7174,#1781);
#1437=LINE('',#7177,#1782);
#1438=LINE('',#7179,#1783);
#1439=LINE('',#7180,#1784);
#1440=LINE('',#7183,#1785);
#1441=LINE('',#7185,#1786);
#1442=LINE('',#7186,#1787);
#1443=LINE('',#7188,#1788);
#1444=LINE('',#7189,#1789);
#1778=VECTOR('',#5730,1.);
#1779=VECTOR('',#5731,1.);
#1780=VECTOR('',#5732,1.);
#1781=VECTOR('',#5733,1.);
#1782=VECTOR('',#5736,1.);
#1783=VECTOR('',#5737,1.);
#1784=VECTOR('',#5738,1.);
#1785=VECTOR('',#5741,1.);
#1786=VECTOR('',#5742,1.);
#1787=VECTOR('',#5743,1.);
#1788=VECTOR('',#5746,1.);
#1789=VECTOR('',#5747,1.);
#2300=VERTEX_POINT('',#7167);
#2301=VERTEX_POINT('',#7168);
#2302=VERTEX_POINT('',#7170);
#2303=VERTEX_POINT('',#7172);
#2304=VERTEX_POINT('',#7176);
#2305=VERTEX_POINT('',#7178);
#2306=VERTEX_POINT('',#7182);
#2307=VERTEX_POINT('',#7184);
#2701=EDGE_CURVE('',#2300,#2301,#1433,.T.);
#2702=EDGE_CURVE('',#2301,#2302,#1434,.T.);
#2703=EDGE_CURVE('',#2303,#2302,#1435,.T.);
#2704=EDGE_CURVE('',#2300,#2303,#1436,.T.);
#2705=EDGE_CURVE('',#2304,#2300,#1437,.T.);
#2706=EDGE_CURVE('',#2305,#2303,#1438,.T.);
#2707=EDGE_CURVE('',#2304,#2305,#1439,.T.);
#2708=EDGE_CURVE('',#2306,#2304,#1440,.T.);
#2709=EDGE_CURVE('',#2307,#2305,#1441,.T.);
#2710=EDGE_CURVE('',#2306,#2307,#1442,.T.);
#2711=EDGE_CURVE('',#2301,#2306,#1443,.T.);
#2712=EDGE_CURVE('',#2302,#2307,#1444,.T.);
#3315=ORIENTED_EDGE('',*,*,#2701,.T.);
#3316=ORIENTED_EDGE('',*,*,#2702,.T.);
#3317=ORIENTED_EDGE('',*,*,#2703,.F.);
#3318=ORIENTED_EDGE('',*,*,#2704,.F.);
#3319=ORIENTED_EDGE('',*,*,#2705,.T.);
#3320=ORIENTED_EDGE('',*,*,#2704,.T.);
#3321=ORIENTED_EDGE('',*,*,#2706,.F.);
#3322=ORIENTED_EDGE('',*,*,#2707,.F.);
#3323=ORIENTED_EDGE('',*,*,#2708,.T.);
#3324=ORIENTED_EDGE('',*,*,#2707,.T.);
#3325=ORIENTED_EDGE('',*,*,#2709,.F.);
#3326=ORIENTED_EDGE('',*,*,#2710,.F.);
#3327=ORIENTED_EDGE('',*,*,#2711,.T.);
#3328=ORIENTED_EDGE('',*,*,#2710,.T.);
#3329=ORIENTED_EDGE('',*,*,#2712,.F.);
#3330=ORIENTED_EDGE('',*,*,#2702,.F.);
#3331=ORIENTED_EDGE('',*,*,#2712,.T.);
#3332=ORIENTED_EDGE('',*,*,#2709,.T.);
#3333=ORIENTED_EDGE('',*,*,#2706,.T.);
#3334=ORIENTED_EDGE('',*,*,#2703,.T.);
#3335=ORIENTED_EDGE('',*,*,#2711,.F.);
#3336=ORIENTED_EDGE('',*,*,#2701,.F.);
#3337=ORIENTED_EDGE('',*,*,#2705,.F.);
#3338=ORIENTED_EDGE('',*,*,#2708,.F.);
#4496=ADVANCED_FACE('',(#760),#582,.T.);
#4497=ADVANCED_FACE('',(#761),#583,.T.);
#4498=ADVANCED_FACE('',(#762),#584,.T.);
#4499=ADVANCED_FACE('',(#763),#585,.T.);
#4500=ADVANCED_FACE('',(#764),#586,.T.);
#4501=ADVANCED_FACE('',(#765),#587,.F.);
#4754=CLOSED_SHELL('',(#4496,#4497,#4498,#4499,#4500,#4501));
#5121=AXIS2_PLACEMENT_3D('',#7165,#5726,#5727);
#5122=AXIS2_PLACEMENT_3D('',#7166,#5728,#5729);
#5123=AXIS2_PLACEMENT_3D('',#7175,#5734,#5735);
#5124=AXIS2_PLACEMENT_3D('',#7181,#5739,#5740);
#5125=AXIS2_PLACEMENT_3D('',#7187,#5744,#5745);
#5126=AXIS2_PLACEMENT_3D('',#7190,#5748,#5749);
#5127=AXIS2_PLACEMENT_3D('',#7191,#5750,#5751);
#5726=DIRECTION('axis',(0.,0.,1.));
#5727=DIRECTION('refdir',(1.,0.,0.));
#5728=DIRECTION('center_axis',(0.,1.,0.));
#5729=DIRECTION('ref_axis',(-1.,0.,0.));
#5730=DIRECTION('',(-1.,0.,0.));
#5731=DIRECTION('',(0.,0.,1.));
#5732=DIRECTION('',(-1.,0.,0.));
#5733=DIRECTION('',(0.,0.,1.));
#5734=DIRECTION('center_axis',(1.,0.,0.));
#5735=DIRECTION('ref_axis',(0.,1.,0.));
#5736=DIRECTION('',(0.,1.,0.));
#5737=DIRECTION('',(0.,1.,0.));
#5738=DIRECTION('',(0.,0.,1.));
#5739=DIRECTION('center_axis',(0.,-1.,0.));
#5740=DIRECTION('ref_axis',(1.,0.,0.));
#5741=DIRECTION('',(1.,0.,0.));
#5742=DIRECTION('',(1.,0.,0.));
#5743=DIRECTION('',(0.,0.,1.));
#5744=DIRECTION('center_axis',(-1.,0.,0.));
#5745=DIRECTION('ref_axis',(0.,-1.,0.));
#5746=DIRECTION('',(0.,-1.,0.));
#5747=DIRECTION('',(0.,-1.,0.));
#5748=DIRECTION('center_axis',(0.,0.,1.));
#5749=DIRECTION('ref_axis',(1.,0.,0.));
#5750=DIRECTION('center_axis',(0.,0.,1.));
#5751=DIRECTION('ref_axis',(1.,0.,0.));
#7165=CARTESIAN_POINT('',(0.,0.,0.));
#7166=CARTESIAN_POINT('Origin',(9.,24.,-0.3));
#7167=CARTESIAN_POINT('',(9.,24.,-0.3));
#7168=CARTESIAN_POINT('',(-9.,24.,-0.3));
#7169=CARTESIAN_POINT('',(9.,24.,-0.3));
#7170=CARTESIAN_POINT('',(-9.,24.,0.));
#7171=CARTESIAN_POINT('',(-9.,24.,-0.3));
#7172=CARTESIAN_POINT('',(9.,24.,0.));
#7173=CARTESIAN_POINT('',(9.,24.,0.));
#7174=CARTESIAN_POINT('',(9.,24.,-0.3));
#7175=CARTESIAN_POINT('Origin',(9.,23.,-0.3));
#7176=CARTESIAN_POINT('',(9.,23.,-0.3));
#7177=CARTESIAN_POINT('',(9.,23.,-0.3));
#7178=CARTESIAN_POINT('',(9.,23.,0.));
#7179=CARTESIAN_POINT('',(9.,23.,0.));
#7180=CARTESIAN_POINT('',(9.,23.,-0.3));
#7181=CARTESIAN_POINT('Origin',(-9.,23.,-0.3));
#7182=CARTESIAN_POINT('',(-9.,23.,-0.3));
#7183=CARTESIAN_POINT('',(-9.,23.,-0.3));
#7184=CARTESIAN_POINT('',(-9.,23.,0.));
#7185=CARTESIAN_POINT('',(-9.,23.,0.));
#7186=CARTESIAN_POINT('',(-9.,23.,-0.3));
#7187=CARTESIAN_POINT('Origin',(-9.,24.,-0.3));
#7188=CARTESIAN_POINT('',(-9.,24.,-0.3));
#7189=CARTESIAN_POINT('',(-9.,24.,0.));
#7190=CARTESIAN_POINT('Origin',(0.,23.5,0.));
#7191=CARTESIAN_POINT('Origin',(0.,23.5,-0.3));
#9080=UNCERTAINTY_MEASURE_WITH_UNIT(LENGTH_MEASURE(0.001),#9142,
'DISTANCE_ACCURACY_VALUE',
'Maximum model space distance between geometric entities at asserted c
onnectivities');
#9108=UNCERTAINTY_MEASURE_WITH_UNIT(LENGTH_MEASURE(0.001),#9142,
'DISTANCE_ACCURACY_VALUE',
'Maximum model space distance between geometric entities at asserted c
onnectivities');
#9113=(
GEOMETRIC_REPRESENTATION_CONTEXT(3)
GLOBAL_UNCERTAINTY_ASSIGNED_CONTEXT((#9080))
GLOBAL_UNIT_ASSIGNED_CONTEXT((#9142,#9144,#9145))
REPRESENTATION_CONTEXT('','3D')
);
#9141=(
GEOMETRIC_REPRESENTATION_CONTEXT(3)
GLOBAL_UNCERTAINTY_ASSIGNED_CONTEXT((#9108))
GLOBAL_UNIT_ASSIGNED_CONTEXT((#9142,#9144,#9145))
REPRESENTATION_CONTEXT('','3D')
);
#9142=(
LENGTH_UNIT()
NAMED_UNIT(*)
SI_UNIT(.CENTI.,.METRE.)
);
#9144=(
NAMED_UNIT(*)
PLANE_ANGLE_UNIT()
SI_UNIT($,.RADIAN.)
);
#9145=(
NAMED_UNIT(*)
SI_UNIT($,.STERADIAN.)
SOLID_ANGLE_UNIT()
);
#9150=SHAPE_DEFINITION_REPRESENTATION(#9182,#9278);
#9182=PRODUCT_DEFINITION_SHAPE('',$,#9311);
#9278=SHAPE_REPRESENTATION('',(#5121),#9113);
#9306=PRODUCT_DEFINITION_CONTEXT('part definition',#9404,'design');
#9311=PRODUCT_DEFINITION('Bonded pad (1)','Bonded pad (1)',#9343,#9306);
#9343=PRODUCT_DEFINITION_FORMATION('',$,#9410);
#9404=APPLICATION_CONTEXT(
'Core Data for Automotive Mechanical Design Process');
#9405=PRODUCT_CONTEXT('part definition',#9404,'mechanical');
#9410=PRODUCT('Bonded pad (1)','Bonded pad (1)','Bonded pad (1)',(#9405));
#9508=COLOUR_RGB('Off White',0.89,0.88,0.83);
#9509=FILL_AREA_STYLE_COLOUR('',#9508);
#9510=FILL_AREA_STYLE('',(#9509));
#9511=SURFACE_STYLE_FILL_AREA(#9510);
#9512=SURFACE_SIDE_STYLE('',(#9511));
#9513=SURFACE_STYLE_USAGE(.BOTH.,#9512);
#9514=PRESENTATION_STYLE_ASSIGNMENT((#9513));
ENDSEC;
END-ISO-10303-21;
